ISO-10303-21;
HEADER;
/* Generated by software containing ST-Developer
 * from STEP Tools, Inc. (www.steptools.com) 
 */

FILE_DESCRIPTION(
/* description */ ('Guided pneumatic stop gate'),
/* implementation_level */ '2;1');

FILE_NAME(
/* name */ 'Cylinder foot screw.step',
/* time_stamp */ '2026-10-27T21:43:45-07:00',
/* author */ (''),
/* organization */ (''),
/* preprocessor_version */ 'ST-DEVELOPER v20.2',
/* originating_system */ 'Autodesk Translation Framework v15.17.0.0',
/* authorisation */ '');

FILE_SCHEMA (('AUTOMOTIVE_DESIGN { 1 0 10303 214 3 1 1 }'));
ENDSEC;

DATA;
#10=MECHANICAL_DESIGN_GEOMETRIC_PRESENTATION_REPRESENTATION('',(#562),#14392);
#417=ORIENTED_CLOSED_SHELL('',*,#7904,.F.);
#421=BREP_WITH_VOIDS('Body1',#7905,(#417));
#437=CONICAL_SURFACE('',#9073,0.4,0.785398163397448);
#438=CONICAL_SURFACE('',#9077,0.41,0.785398163397448);
#439=CONICAL_SURFACE('',#9081,0.26,0.463647609000806);
#440=CONICAL_SURFACE('',#9085,0.225,0.785398163397448);
#478=SHAPE_REPRESENTATION_RELATIONSHIP('SRR','None',#14614,#520);
#520=ADVANCED_BREP_SHAPE_REPRESENTATION('',(#421),#14376);
#562=STYLED_ITEM('',(#14898),#421);
#789=FACE_BOUND('',#2115,.T.);
#790=FACE_BOUND('',#2123,.T.);
#1031=PLANE('',#9057);
#1032=PLANE('',#9058);
#1033=PLANE('',#9059);
#1034=PLANE('',#9060);
#1035=PLANE('',#9061);
#1036=PLANE('',#9062);
#1037=PLANE('',#9063);
#1038=PLANE('',#9064);
#1039=PLANE('',#9065);
#1040=PLANE('',#9070);
#1041=PLANE('',#9071);
#1042=PLANE('',#9079);
#1457=FACE_OUTER_BOUND('',#2106,.T.);
#1458=FACE_OUTER_BOUND('',#2107,.T.);
#1459=FACE_OUTER_BOUND('',#2108,.T.);
#1460=FACE_OUTER_BOUND('',#2109,.T.);
#1461=FACE_OUTER_BOUND('',#2110,.T.);
#1462=FACE_OUTER_BOUND('',#2111,.T.);
#1463=FACE_OUTER_BOUND('',#2112,.T.);
#1464=FACE_OUTER_BOUND('',#2113,.T.);
#1465=FACE_OUTER_BOUND('',#2114,.T.);
#1466=FACE_OUTER_BOUND('',#2116,.T.);
#1467=FACE_OUTER_BOUND('',#2117,.T.);
#1468=FACE_OUTER_BOUND('',#2118,.T.);
#1469=FACE_OUTER_BOUND('',#2119,.T.);
#1470=FACE_OUTER_BOUND('',#2120,.T.);
#1471=FACE_OUTER_BOUND('',#2121,.T.);
#1472=FACE_OUTER_BOUND('',#2122,.T.);
#1473=FACE_OUTER_BOUND('',#2124,.T.);
#1474=FACE_OUTER_BOUND('',#2125,.T.);
#1475=FACE_OUTER_BOUND('',#2126,.T.);
#2106=EDGE_LOOP('',(#6702,#6703,#6704,#6705));
#2107=EDGE_LOOP('',(#6706,#6707,#6708,#6709));
#2108=EDGE_LOOP('',(#6710,#6711,#6712,#6713));
#2109=EDGE_LOOP('',(#6714,#6715,#6716,#6717));
#2110=EDGE_LOOP('',(#6718,#6719,#6720,#6721));
#2111=EDGE_LOOP('',(#6722,#6723,#6724,#6725));
#2112=EDGE_LOOP('',(#6726,#6727,#6728,#6729,#6730,#6731));
#2113=EDGE_LOOP('',(#6732,#6733,#6734,#6735,#6736,#6737));
#2114=EDGE_LOOP('',(#6738));
#2115=EDGE_LOOP('',(#6739));
#2116=EDGE_LOOP('',(#6740,#6741,#6742,#6743));
#2117=EDGE_LOOP('',(#6744));
#2118=EDGE_LOOP('',(#6745));
#2119=EDGE_LOOP('',(#6746,#6747,#6748,#6749));
#2120=EDGE_LOOP('',(#6750,#6751,#6752,#6753));
#2121=EDGE_LOOP('',(#6754,#6755,#6756,#6757));
#2122=EDGE_LOOP('',(#6758));
#2123=EDGE_LOOP('',(#6759));
#2124=EDGE_LOOP('',(#6760,#6761,#6762,#6763));
#2125=EDGE_LOOP('',(#6764,#6765,#6766,#6767));
#2126=EDGE_LOOP('',(#6768,#6769,#6770,#6771));
#2661=LINE('',#13461,#3206);
#2662=LINE('',#13463,#3207);
#2663=LINE('',#13465,#3208);
#2664=LINE('',#13466,#3209);
#2665=LINE('',#13469,#3210);
#2666=LINE('',#13471,#3211);
#2667=LINE('',#13472,#3212);
#2668=LINE('',#13475,#3213);
#2669=LINE('',#13477,#3214);
#2670=LINE('',#13478,#3215);
#2671=LINE('',#13481,#3216);
#2672=LINE('',#13483,#3217);
#2673=LINE('',#13484,#3218);
#2674=LINE('',#13487,#3219);
#2675=LINE('',#13489,#3220);
#2676=LINE('',#13490,#3221);
#2677=LINE('',#13492,#3222);
#2678=LINE('',#13493,#3223);
#2679=LINE('',#13503,#3224);
#2680=LINE('',#13512,#3225);
#2681=LINE('',#13516,#3226);
#2682=LINE('',#13520,#3227);
#2683=LINE('',#13527,#3228);
#2684=LINE('',#13531,#3229);
#2685=LINE('',#13533,#3230);
#3206=VECTOR('',#11112,1.);
#3207=VECTOR('',#11113,1.);
#3208=VECTOR('',#11114,1.);
#3209=VECTOR('',#11115,1.);
#3210=VECTOR('',#11118,1.);
#3211=VECTOR('',#11119,1.);
#3212=VECTOR('',#11120,1.);
#3213=VECTOR('',#11123,1.);
#3214=VECTOR('',#11124,1.);
#3215=VECTOR('',#11125,1.);
#3216=VECTOR('',#11128,1.);
#3217=VECTOR('',#11129,1.);
#3218=VECTOR('',#11130,1.);
#3219=VECTOR('',#11133,1.);
#3220=VECTOR('',#11134,1.);
#3221=VECTOR('',#11135,1.);
#3222=VECTOR('',#11138,1.);
#3223=VECTOR('',#11139,1.);
#3224=VECTOR('',#11152,0.25);
#3225=VECTOR('',#11165,0.4);
#3226=VECTOR('',#11170,0.425);
#3227=VECTOR('',#11175,0.41);
#3228=VECTOR('',#11184,0.26);
#3229=VECTOR('',#11189,0.25);
#3230=VECTOR('',#11192,0.225);
#3652=CIRCLE('',#9066,0.25);
#3653=CIRCLE('',#9067,0.21);
#3654=CIRCLE('',#9069,0.25);
#3655=CIRCLE('',#9072,0.375);
#3656=CIRCLE('',#9074,0.425);
#3657=CIRCLE('',#9076,0.425);
#3658=CIRCLE('',#9078,0.395);
#3659=CIRCLE('',#9080,0.27);
#3660=CIRCLE('',#9082,0.24505);
#3661=CIRCLE('',#9084,0.24505);
#4183=VERTEX_POINT('',#13459);
#4184=VERTEX_POINT('',#13460);
#4185=VERTEX_POINT('',#13462);
#4186=VERTEX_POINT('',#13464);
#4187=VERTEX_POINT('',#13468);
#4188=VERTEX_POINT('',#13470);
#4189=VERTEX_POINT('',#13474);
#4190=VERTEX_POINT('',#13476);
#4191=VERTEX_POINT('',#13480);
#4192=VERTEX_POINT('',#13482);
#4193=VERTEX_POINT('',#13486);
#4194=VERTEX_POINT('',#13488);
#4195=VERTEX_POINT('',#13497);
#4196=VERTEX_POINT('',#13499);
#4197=VERTEX_POINT('',#13502);
#4198=VERTEX_POINT('',#13507);
#4199=VERTEX_POINT('',#13510);
#4200=VERTEX_POINT('',#13514);
#4201=VERTEX_POINT('',#13518);
#4202=VERTEX_POINT('',#13522);
#4203=VERTEX_POINT('',#13525);
#4204=VERTEX_POINT('',#13529);
#5049=EDGE_CURVE('',#4183,#4184,#2661,.T.);
#5050=EDGE_CURVE('',#4184,#4185,#2662,.T.);
#5051=EDGE_CURVE('',#4185,#4186,#2663,.T.);
#5052=EDGE_CURVE('',#4183,#4186,#2664,.T.);
#5053=EDGE_CURVE('',#4184,#4187,#2665,.T.);
#5054=EDGE_CURVE('',#4187,#4188,#2666,.T.);
#5055=EDGE_CURVE('',#4188,#4185,#2667,.T.);
#5056=EDGE_CURVE('',#4187,#4189,#2668,.T.);
#5057=EDGE_CURVE('',#4189,#4190,#2669,.T.);
#5058=EDGE_CURVE('',#4190,#4188,#2670,.T.);
#5059=EDGE_CURVE('',#4189,#4191,#2671,.T.);
#5060=EDGE_CURVE('',#4191,#4192,#2672,.T.);
#5061=EDGE_CURVE('',#4192,#4190,#2673,.T.);
#5062=EDGE_CURVE('',#4191,#4193,#2674,.T.);
#5063=EDGE_CURVE('',#4193,#4194,#2675,.T.);
#5064=EDGE_CURVE('',#4194,#4192,#2676,.T.);
#5065=EDGE_CURVE('',#4193,#4183,#2677,.T.);
#5066=EDGE_CURVE('',#4186,#4194,#2678,.T.);
#5067=EDGE_CURVE('',#4195,#4195,#3652,.T.);
#5068=EDGE_CURVE('',#4196,#4196,#3653,.T.);
#5069=EDGE_CURVE('',#4195,#4197,#2679,.T.);
#5070=EDGE_CURVE('',#4197,#4197,#3654,.T.);
#5071=EDGE_CURVE('',#4198,#4198,#3655,.T.);
#5072=EDGE_CURVE('',#4199,#4199,#3656,.T.);
#5073=EDGE_CURVE('',#4199,#4198,#2680,.T.);
#5074=EDGE_CURVE('',#4200,#4200,#3657,.T.);
#5075=EDGE_CURVE('',#4200,#4199,#2681,.T.);
#5076=EDGE_CURVE('',#4201,#4201,#3658,.T.);
#5077=EDGE_CURVE('',#4201,#4200,#2682,.T.);
#5078=EDGE_CURVE('',#4202,#4202,#3659,.T.);
#5079=EDGE_CURVE('',#4203,#4203,#3660,.F.);
#5080=EDGE_CURVE('',#4203,#4202,#2683,.T.);
#5081=EDGE_CURVE('',#4204,#4204,#3661,.F.);
#5082=EDGE_CURVE('',#4204,#4203,#2684,.T.);
#5083=EDGE_CURVE('',#4196,#4204,#2685,.T.);
#6702=ORIENTED_EDGE('',*,*,#5049,.T.);
#6703=ORIENTED_EDGE('',*,*,#5050,.T.);
#6704=ORIENTED_EDGE('',*,*,#5051,.T.);
#6705=ORIENTED_EDGE('',*,*,#5052,.F.);
#6706=ORIENTED_EDGE('',*,*,#5053,.T.);
#6707=ORIENTED_EDGE('',*,*,#5054,.T.);
#6708=ORIENTED_EDGE('',*,*,#5055,.T.);
#6709=ORIENTED_EDGE('',*,*,#5050,.F.);
#6710=ORIENTED_EDGE('',*,*,#5056,.T.);
#6711=ORIENTED_EDGE('',*,*,#5057,.T.);
#6712=ORIENTED_EDGE('',*,*,#5058,.T.);
#6713=ORIENTED_EDGE('',*,*,#5054,.F.);
#6714=ORIENTED_EDGE('',*,*,#5059,.T.);
#6715=ORIENTED_EDGE('',*,*,#5060,.T.);
#6716=ORIENTED_EDGE('',*,*,#5061,.T.);
#6717=ORIENTED_EDGE('',*,*,#5057,.F.);
#6718=ORIENTED_EDGE('',*,*,#5062,.T.);
#6719=ORIENTED_EDGE('',*,*,#5063,.T.);
#6720=ORIENTED_EDGE('',*,*,#5064,.T.);
#6721=ORIENTED_EDGE('',*,*,#5060,.F.);
#6722=ORIENTED_EDGE('',*,*,#5065,.T.);
#6723=ORIENTED_EDGE('',*,*,#5052,.T.);
#6724=ORIENTED_EDGE('',*,*,#5066,.T.);
#6725=ORIENTED_EDGE('',*,*,#5063,.F.);
#6726=ORIENTED_EDGE('',*,*,#5065,.F.);
#6727=ORIENTED_EDGE('',*,*,#5062,.F.);
#6728=ORIENTED_EDGE('',*,*,#5059,.F.);
#6729=ORIENTED_EDGE('',*,*,#5056,.F.);
#6730=ORIENTED_EDGE('',*,*,#5053,.F.);
#6731=ORIENTED_EDGE('',*,*,#5049,.F.);
#6732=ORIENTED_EDGE('',*,*,#5066,.F.);
#6733=ORIENTED_EDGE('',*,*,#5051,.F.);
#6734=ORIENTED_EDGE('',*,*,#5055,.F.);
#6735=ORIENTED_EDGE('',*,*,#5058,.F.);
#6736=ORIENTED_EDGE('',*,*,#5061,.F.);
#6737=ORIENTED_EDGE('',*,*,#5064,.F.);
#6738=ORIENTED_EDGE('',*,*,#5067,.T.);
#6739=ORIENTED_EDGE('',*,*,#5068,.F.);
#6740=ORIENTED_EDGE('',*,*,#5067,.F.);
#6741=ORIENTED_EDGE('',*,*,#5069,.T.);
#6742=ORIENTED_EDGE('',*,*,#5070,.T.);
#6743=ORIENTED_EDGE('',*,*,#5069,.F.);
#6744=ORIENTED_EDGE('',*,*,#5070,.F.);
#6745=ORIENTED_EDGE('',*,*,#5071,.F.);
#6746=ORIENTED_EDGE('',*,*,#5072,.F.);
#6747=ORIENTED_EDGE('',*,*,#5073,.T.);
#6748=ORIENTED_EDGE('',*,*,#5071,.T.);
#6749=ORIENTED_EDGE('',*,*,#5073,.F.);
#6750=ORIENTED_EDGE('',*,*,#5074,.F.);
#6751=ORIENTED_EDGE('',*,*,#5075,.T.);
#6752=ORIENTED_EDGE('',*,*,#5072,.T.);
#6753=ORIENTED_EDGE('',*,*,#5075,.F.);
#6754=ORIENTED_EDGE('',*,*,#5076,.F.);
#6755=ORIENTED_EDGE('',*,*,#5077,.T.);
#6756=ORIENTED_EDGE('',*,*,#5074,.T.);
#6757=ORIENTED_EDGE('',*,*,#5077,.F.);
#6758=ORIENTED_EDGE('',*,*,#5076,.T.);
#6759=ORIENTED_EDGE('',*,*,#5078,.F.);
#6760=ORIENTED_EDGE('',*,*,#5079,.F.);
#6761=ORIENTED_EDGE('',*,*,#5080,.T.);
#6762=ORIENTED_EDGE('',*,*,#5078,.T.);
#6763=ORIENTED_EDGE('',*,*,#5080,.F.);
#6764=ORIENTED_EDGE('',*,*,#5081,.F.);
#6765=ORIENTED_EDGE('',*,*,#5082,.T.);
#6766=ORIENTED_EDGE('',*,*,#5079,.T.);
#6767=ORIENTED_EDGE('',*,*,#5082,.F.);
#6768=ORIENTED_EDGE('',*,*,#5068,.T.);
#6769=ORIENTED_EDGE('',*,*,#5083,.T.);
#6770=ORIENTED_EDGE('',*,*,#5081,.T.);
#6771=ORIENTED_EDGE('',*,*,#5083,.F.);
#7367=CYLINDRICAL_SURFACE('',#9068,0.25);
#7368=CYLINDRICAL_SURFACE('',#9075,0.425);
#7369=CYLINDRICAL_SURFACE('',#9083,0.24505);
#7739=ADVANCED_FACE('',(#1457),#1031,.F.);
#7740=ADVANCED_FACE('',(#1458),#1032,.F.);
#7741=ADVANCED_FACE('',(#1459),#1033,.F.);
#7742=ADVANCED_FACE('',(#1460),#1034,.F.);
#7743=ADVANCED_FACE('',(#1461),#1035,.F.);
#7744=ADVANCED_FACE('',(#1462),#1036,.F.);
#7745=ADVANCED_FACE('',(#1463),#1037,.F.);
#7746=ADVANCED_FACE('',(#1464),#1038,.F.);
#7747=ADVANCED_FACE('',(#1465,#789),#1039,.T.);
#7748=ADVANCED_FACE('',(#1466),#7367,.T.);
#7749=ADVANCED_FACE('',(#1467),#1040,.F.);
#7750=ADVANCED_FACE('',(#1468),#1041,.T.);
#7751=ADVANCED_FACE('',(#1469),#437,.T.);
#7752=ADVANCED_FACE('',(#1470),#7368,.T.);
#7753=ADVANCED_FACE('',(#1471),#438,.T.);
#7754=ADVANCED_FACE('',(#1472,#790),#1042,.T.);
#7755=ADVANCED_FACE('',(#1473),#439,.T.);
#7756=ADVANCED_FACE('',(#1474),#7369,.T.);
#7757=ADVANCED_FACE('',(#1475),#440,.T.);
#7904=CLOSED_SHELL('',(#7739,#7740,#7741,#7742,#7743,#7744,#7745,#7746));
#7905=CLOSED_SHELL('',(#7747,#7748,#7749,#7750,#7751,#7752,#7753,#7754,
#7755,#7756,#7757));
#9056=AXIS2_PLACEMENT_3D('',#13457,#11108,#11109);
#9057=AXIS2_PLACEMENT_3D('',#13458,#11110,#11111);
#9058=AXIS2_PLACEMENT_3D('',#13467,#11116,#11117);
#9059=AXIS2_PLACEMENT_3D('',#13473,#11121,#11122);
#9060=AXIS2_PLACEMENT_3D('',#13479,#11126,#11127);
#9061=AXIS2_PLACEMENT_3D('',#13485,#11131,#11132);
#9062=AXIS2_PLACEMENT_3D('',#13491,#11136,#11137);
#9063=AXIS2_PLACEMENT_3D('',#13494,#11140,#11141);
#9064=AXIS2_PLACEMENT_3D('',#13495,#11142,#11143);
#9065=AXIS2_PLACEMENT_3D('',#13496,#11144,#11145);
#9066=AXIS2_PLACEMENT_3D('',#13498,#11146,#11147);
#9067=AXIS2_PLACEMENT_3D('',#13500,#11148,#11149);
#9068=AXIS2_PLACEMENT_3D('',#13501,#11150,#11151);
#9069=AXIS2_PLACEMENT_3D('',#13504,#11153,#11154);
#9070=AXIS2_PLACEMENT_3D('',#13505,#11155,#11156);
#9071=AXIS2_PLACEMENT_3D('',#13506,#11157,#11158);
#9072=AXIS2_PLACEMENT_3D('',#13508,#11159,#11160);
#9073=AXIS2_PLACEMENT_3D('',#13509,#11161,#11162);
#9074=AXIS2_PLACEMENT_3D('',#13511,#11163,#11164);
#9075=AXIS2_PLACEMENT_3D('',#13513,#11166,#11167);
#9076=AXIS2_PLACEMENT_3D('',#13515,#11168,#11169);
#9077=AXIS2_PLACEMENT_3D('',#13517,#11171,#11172);
#9078=AXIS2_PLACEMENT_3D('',#13519,#11173,#11174);
#9079=AXIS2_PLACEMENT_3D('',#13521,#11176,#11177);
#9080=AXIS2_PLACEMENT_3D('',#13523,#11178,#11179);
#9081=AXIS2_PLACEMENT_3D('',#13524,#11180,#11181);
#9082=AXIS2_PLACEMENT_3D('',#13526,#11182,#11183);
#9083=AXIS2_PLACEMENT_3D('',#13528,#11185,#11186);
#9084=AXIS2_PLACEMENT_3D('',#13530,#11187,#11188);
#9085=AXIS2_PLACEMENT_3D('',#13532,#11190,#11191);
#11108=DIRECTION('axis',(0.,0.,1.));
#11109=DIRECTION('refdir',(1.,0.,0.));
#11110=DIRECTION('center_axis',(0.866025403784439,0.,-0.5));
#11111=DIRECTION('ref_axis',(0.5,0.,0.866025403784439));
#11112=DIRECTION('',(-0.5,0.,-0.866025403784439));
#11113=DIRECTION('',(0.,-1.,0.));
#11114=DIRECTION('',(0.5,0.,0.866025403784439));
#11115=DIRECTION('',(0.,-1.,0.));
#11116=DIRECTION('center_axis',(1.20185167898973E-16,0.,-1.));
#11117=DIRECTION('ref_axis',(1.,0.,1.20185167898973E-16));
#11118=DIRECTION('',(-1.,0.,-1.20185167898973E-16));
#11119=DIRECTION('',(0.,-1.,0.));
#11120=DIRECTION('',(1.,0.,1.20185167898973E-16));
#11121=DIRECTION('center_axis',(-0.866025403784439,0.,-0.5));
#11122=DIRECTION('ref_axis',(0.5,0.,-0.866025403784439));
#11123=DIRECTION('',(-0.5,0.,0.866025403784439));
#11124=DIRECTION('',(0.,-1.,0.));
#11125=DIRECTION('',(0.5,0.,-0.866025403784439));
#11126=DIRECTION('center_axis',(-0.866025403784439,0.,0.5));
#11127=DIRECTION('ref_axis',(-0.5,0.,-0.866025403784439));
#11128=DIRECTION('',(0.5,0.,0.866025403784439));
#11129=DIRECTION('',(0.,-1.,0.));
#11130=DIRECTION('',(-0.5,0.,-0.866025403784439));
#11131=DIRECTION('center_axis',(-2.40370335797945E-16,0.,1.));
#11132=DIRECTION('ref_axis',(-1.,0.,-2.40370335797945E-16));
#11133=DIRECTION('',(1.,0.,2.40370335797945E-16));
#11134=DIRECTION('',(0.,-1.,0.));
#11135=DIRECTION('',(-1.,0.,-2.40370335797945E-16));
#11136=DIRECTION('center_axis',(0.866025403784439,0.,0.5));
#11137=DIRECTION('ref_axis',(-0.5,0.,0.866025403784439));
#11138=DIRECTION('',(0.5,0.,-0.866025403784439));
#11139=DIRECTION('',(-0.5,0.,0.866025403784439));
#11140=DIRECTION('center_axis',(0.,1.,0.));
#11141=DIRECTION('ref_axis',(1.,0.,0.));
#11142=DIRECTION('center_axis',(0.,-1.,0.));
#11143=DIRECTION('ref_axis',(0.,0.,-1.));
#11144=DIRECTION('center_axis',(0.,1.,0.));
#11145=DIRECTION('ref_axis',(1.,0.,0.));
#11146=DIRECTION('center_axis',(0.,1.,0.));
#11147=DIRECTION('ref_axis',(1.,0.,0.));
#11148=DIRECTION('center_axis',(0.,1.,0.));
#11149=DIRECTION('ref_axis',(1.,0.,0.));
#11150=DIRECTION('center_axis',(0.,1.,0.));
#11151=DIRECTION('ref_axis',(1.,0.,0.));
#11152=DIRECTION('',(0.,-1.,0.));
#11153=DIRECTION('center_axis',(0.,1.,0.));
#11154=DIRECTION('ref_axis',(1.,0.,0.));
#11155=DIRECTION('center_axis',(0.,1.,0.));
#11156=DIRECTION('ref_axis',(1.,0.,0.));
#11157=DIRECTION('center_axis',(0.,1.,0.));
#11158=DIRECTION('ref_axis',(0.,0.,1.));
#11159=DIRECTION('center_axis',(0.,-1.,0.));
#11160=DIRECTION('ref_axis',(1.,0.,0.));
#11161=DIRECTION('center_axis',(0.,-1.,0.));
#11162=DIRECTION('ref_axis',(1.,0.,0.));
#11163=DIRECTION('center_axis',(0.,-1.,0.));
#11164=DIRECTION('ref_axis',(1.,0.,0.));
#11165=DIRECTION('',(0.707106781186548,0.707106781186547,8.65956056235493E-17));
#11166=DIRECTION('center_axis',(0.,-1.,0.));
#11167=DIRECTION('ref_axis',(1.,0.,0.));
#11168=DIRECTION('center_axis',(0.,-1.,0.));
#11169=DIRECTION('ref_axis',(1.,0.,0.));
#11170=DIRECTION('',(0.,1.,0.));
#11171=DIRECTION('center_axis',(0.,1.,0.));
#11172=DIRECTION('ref_axis',(1.,0.,0.));
#11173=DIRECTION('center_axis',(0.,-1.,0.));
#11174=DIRECTION('ref_axis',(1.,0.,0.));
#11175=DIRECTION('',(-0.707106781186547,0.707106781186548,-8.65956056235493E-17));
#11176=DIRECTION('center_axis',(0.,-1.,0.));
#11177=DIRECTION('ref_axis',(0.,0.,-1.));
#11178=DIRECTION('center_axis',(0.,-1.,0.));
#11179=DIRECTION('ref_axis',(1.,0.,0.));
#11180=DIRECTION('center_axis',(0.,1.,0.));
#11181=DIRECTION('ref_axis',(1.,0.,0.));
#11182=DIRECTION('center_axis',(0.,1.,0.));
#11183=DIRECTION('ref_axis',(1.,0.,0.));
#11184=DIRECTION('',(-0.447213595499958,0.894427190999916,-5.47678698264203E-17));
#11185=DIRECTION('center_axis',(0.,-1.,0.));
#11186=DIRECTION('ref_axis',(1.,0.,0.));
#11187=DIRECTION('center_axis',(0.,1.,0.));
#11188=DIRECTION('ref_axis',(1.,0.,0.));
#11189=DIRECTION('',(0.,1.,0.));
#11190=DIRECTION('center_axis',(0.,1.,0.));
#11191=DIRECTION('ref_axis',(1.,0.,0.));
#11192=DIRECTION('',(-0.707106781186547,0.707106781186548,-8.65956056235493E-17));
#13457=CARTESIAN_POINT('',(0.,0.,0.));
#13458=CARTESIAN_POINT('Origin',(0.115470053837925,-0.5,-0.2));
#13459=CARTESIAN_POINT('',(0.23094010767585,-0.5,0.));
#13460=CARTESIAN_POINT('',(0.115470053837925,-0.5,-0.2));
#13461=CARTESIAN_POINT('',(0.23094010767585,-0.5,0.));
#13462=CARTESIAN_POINT('',(0.115470053837925,-0.8,-0.2));
#13463=CARTESIAN_POINT('',(0.115470053837925,-0.5,-0.2));
#13464=CARTESIAN_POINT('',(0.23094010767585,-0.8,0.));
#13465=CARTESIAN_POINT('',(0.23094010767585,-0.8,0.));
#13466=CARTESIAN_POINT('',(0.23094010767585,-0.5,0.));
#13467=CARTESIAN_POINT('Origin',(-0.115470053837925,-0.5,-0.2));
#13468=CARTESIAN_POINT('',(-0.115470053837925,-0.5,-0.2));
#13469=CARTESIAN_POINT('',(0.115470053837925,-0.5,-0.2));
#13470=CARTESIAN_POINT('',(-0.115470053837925,-0.8,-0.2));
#13471=CARTESIAN_POINT('',(-0.115470053837925,-0.5,-0.2));
#13472=CARTESIAN_POINT('',(0.115470053837925,-0.8,-0.2));
#13473=CARTESIAN_POINT('Origin',(-0.23094010767585,-0.5,-2.77555756156289E-17));
#13474=CARTESIAN_POINT('',(-0.23094010767585,-0.5,-2.82820063659975E-17));
#13475=CARTESIAN_POINT('',(-0.115470053837925,-0.5,-0.2));
#13476=CARTESIAN_POINT('',(-0.23094010767585,-0.8,-2.77555756156289E-17));
#13477=CARTESIAN_POINT('',(-0.23094010767585,-0.5,-2.82820063659975E-17));
#13478=CARTESIAN_POINT('',(-0.115470053837925,-0.8,-0.2));
#13479=CARTESIAN_POINT('Origin',(-0.115470053837925,-0.5,0.2));
#13480=CARTESIAN_POINT('',(-0.115470053837925,-0.5,0.2));
#13481=CARTESIAN_POINT('',(-0.23094010767585,-0.5,-2.82820063659975E-17));
#13482=CARTESIAN_POINT('',(-0.115470053837925,-0.8,0.2));
#13483=CARTESIAN_POINT('',(-0.115470053837925,-0.5,0.2));
#13484=CARTESIAN_POINT('',(-0.23094010767585,-0.8,-2.82820063659975E-17));
#13485=CARTESIAN_POINT('Origin',(0.115470053837925,-0.5,0.2));
#13486=CARTESIAN_POINT('',(0.115470053837925,-0.5,0.2));
#13487=CARTESIAN_POINT('',(-0.115470053837925,-0.5,0.2));
#13488=CARTESIAN_POINT('',(0.115470053837925,-0.8,0.2));
#13489=CARTESIAN_POINT('',(0.115470053837925,-0.5,0.2));
#13490=CARTESIAN_POINT('',(-0.115470053837925,-0.8,0.2));
#13491=CARTESIAN_POINT('Origin',(0.23094010767585,-0.5,0.));
#13492=CARTESIAN_POINT('',(0.115470053837925,-0.5,0.2));
#13493=CARTESIAN_POINT('',(0.115470053837925,-0.8,0.2));
#13494=CARTESIAN_POINT('Origin',(0.,-0.5,0.));
#13495=CARTESIAN_POINT('Origin',(0.,-0.8,0.));
#13496=CARTESIAN_POINT('Origin',(0.,-1.99,0.));
#13497=CARTESIAN_POINT('',(-0.25,-1.99,3.06161699786838E-17));
#13498=CARTESIAN_POINT('Origin',(0.,-1.99,0.));
#13499=CARTESIAN_POINT('',(-0.21,-1.99,2.57175827820944E-17));
#13500=CARTESIAN_POINT('Origin',(0.,-1.99,0.));
#13501=CARTESIAN_POINT('Origin',(0.,-2.2,0.));
#13502=CARTESIAN_POINT('',(-0.25,-2.2,3.06161699786838E-17));
#13503=CARTESIAN_POINT('',(-0.25,-2.2,3.06161699786838E-17));
#13504=CARTESIAN_POINT('Origin',(0.,-2.2,0.));
#13505=CARTESIAN_POINT('Origin',(0.,-2.2,0.));
#13506=CARTESIAN_POINT('Origin',(0.375,0.5,0.));
#13507=CARTESIAN_POINT('',(-0.375,0.5,-4.59242549680257E-17));
#13508=CARTESIAN_POINT('Origin',(0.,0.5,0.));
#13509=CARTESIAN_POINT('Origin',(0.,0.475,0.));
#13510=CARTESIAN_POINT('',(-0.425,0.45,-5.20474889637625E-17));
#13511=CARTESIAN_POINT('Origin',(0.,0.45,0.));
#13512=CARTESIAN_POINT('',(-0.4,0.475,-4.89858719658941E-17));
#13513=CARTESIAN_POINT('Origin',(0.,0.24,0.));
#13514=CARTESIAN_POINT('',(-0.425,0.0299999999999998,-5.20474889637625E-17));
#13515=CARTESIAN_POINT('Origin',(0.,0.0299999999999998,0.));
#13516=CARTESIAN_POINT('',(-0.425,0.24,-5.20474889637625E-17));
#13517=CARTESIAN_POINT('Origin',(0.,0.0150000000000001,0.));
#13518=CARTESIAN_POINT('',(-0.395,4.85722573273506E-17,-4.83735485663204E-17));
#13519=CARTESIAN_POINT('Origin',(0.,0.,0.));
#13520=CARTESIAN_POINT('',(-0.41,0.0150000000000001,-5.02105187650415E-17));
#13521=CARTESIAN_POINT('Origin',(0.27,0.,0.));
#13522=CARTESIAN_POINT('',(-0.27,0.,-3.30654635769785E-17));
#13523=CARTESIAN_POINT('Origin',(0.,0.,0.));
#13524=CARTESIAN_POINT('Origin',(0.,-0.02,0.));
#13525=CARTESIAN_POINT('',(-0.24505,-0.0498999999999999,3.00099698131059E-17));
#13526=CARTESIAN_POINT('Origin',(0.,-0.0498999999999999,0.));
#13527=CARTESIAN_POINT('',(-0.26,-0.02,-3.18408167778312E-17));
#13528=CARTESIAN_POINT('Origin',(0.,-0.995,0.));
#13529=CARTESIAN_POINT('',(-0.24505,-1.95495,3.00099698131059E-17));
#13530=CARTESIAN_POINT('Origin',(0.,-1.95495,0.));
#13531=CARTESIAN_POINT('',(-0.24505,-0.995,-3.00099698131059E-17));
#13532=CARTESIAN_POINT('Origin',(0.,-1.975,0.));
#13533=CARTESIAN_POINT('',(-0.225,-1.975,-2.75545529808154E-17));
#14328=UNCERTAINTY_MEASURE_WITH_UNIT(LENGTH_MEASURE(0.001),#14393,
'DISTANCE_ACCURACY_VALUE',
'Maximum model space distance between geometric entities at asserted c
onnectivities');
#14344=UNCERTAINTY_MEASURE_WITH_UNIT(LENGTH_MEASURE(0.001),#14393,
'DISTANCE_ACCURACY_VALUE',
'Maximum model space distance between geometric entities at asserted c
onnectivities');
#14376=(
GEOMETRIC_REPRESENTATION_CONTEXT(3)
GLOBAL_UNCERTAINTY_ASSIGNED_CONTEXT((#14328))
GLOBAL_UNIT_ASSIGNED_CONTEXT((#14393,#14395,#14396))
REPRESENTATION_CONTEXT('','3D')
);
#14392=(
GEOMETRIC_REPRESENTATION_CONTEXT(3)
GLOBAL_UNCERTAINTY_ASSIGNED_CONTEXT((#14344))
GLOBAL_UNIT_ASSIGNED_CONTEXT((#14393,#14395,#14396))
REPRESENTATION_CONTEXT('','3D')
);
#14393=(
LENGTH_UNIT()
NAMED_UNIT(*)
SI_UNIT(.CENTI.,.METRE.)
);
#14395=(
NAMED_UNIT(*)
PLANE_ANGLE_UNIT()
SI_UNIT($,.RADIAN.)
);
#14396=(
NAMED_UNIT(*)
SI_UNIT($,.STERADIAN.)
SOLID_ANGLE_UNIT()
);
#14428=SHAPE_DEFINITION_REPRESENTATION(#14479,#14614);
#14479=PRODUCT_DEFINITION_SHAPE('',$,#14662);
#14614=SHAPE_REPRESENTATION('',(#9056),#14376);
#14630=PRODUCT_DEFINITION_CONTEXT('part definition',#14773,'design');
#14662=PRODUCT_DEFINITION('Cylinder foot screw','Cylinder foot screw',#14709,
#14630);
#14709=PRODUCT_DEFINITION_FORMATION('',$,#14806);
#14773=APPLICATION_CONTEXT(
'Core Data for Automotive Mechanical Design Process');
#14774=PRODUCT_CONTEXT('part definition',#14773,'mechanical');
#14806=PRODUCT('Cylinder foot screw','Cylinder foot screw',
'Cylinder foot screw',(#14774));
#14892=COLOUR_RGB('Black',0.12,0.14,0.17);
#14893=FILL_AREA_STYLE_COLOUR('',#14892);
#14894=FILL_AREA_STYLE('',(#14893));
#14895=SURFACE_STYLE_FILL_AREA(#14894);
#14896=SURFACE_SIDE_STYLE('',(#14895));
#14897=SURFACE_STYLE_USAGE(.BOTH.,#14896);
#14898=PRESENTATION_STYLE_ASSIGNMENT((#14897));
ENDSEC;
END-ISO-10303-21;
